ISO-10303-21;
HEADER;
/* Generated by software containing ST-Developer
 * from STEP Tools, Inc. (www.steptools.com) 
 */

FILE_DESCRIPTION(
/* description */ (''),
/* implementation_level */ '2;1');

FILE_NAME(
/* name */ 'Middle_Block_01.step',
/* time_stamp */ '2026-10-23T22:30:33+06:00',
/* author */ (''),
/* organization */ (''),
/* preprocessor_version */ 'ST-DEVELOPER v20.2',
/* originating_system */ 'Autodesk Translation Framework v15.15.0.0',
/* authorisation */ '');

FILE_SCHEMA (('AUTOMOTIVE_DESIGN { 1 0 10303 214 3 1 1 }'));
ENDSEC;

DATA;
#10=MECHANICAL_DESIGN_GEOMETRIC_PRESENTATION_REPRESENTATION('',(#242),#10131);
#135=ELLIPSE('',#6413,1.0823922002924,1.);
#136=ELLIPSE('',#6414,1.08239220029239,1.);
#137=ELLIPSE('',#6416,1.08239220029239,1.);
#138=ELLIPSE('',#6417,1.0823922002924,1.);
#139=ELLIPSE('',#6419,1.0823922002924,1.);
#140=ELLIPSE('',#6421,1.0823922002924,1.);
#141=ELLIPSE('',#6422,1.0823922002924,1.);
#142=ELLIPSE('',#6424,1.08239220029239,1.);
#143=ELLIPSE('',#6427,1.08239220029239,1.);
#144=ELLIPSE('',#6429,1.0823922002924,1.);
#145=ELLIPSE('',#6432,1.08239220029239,1.);
#146=ELLIPSE('',#6434,1.0823922002924,1.);
#147=ELLIPSE('',#6444,1.08239220029239,1.);
#148=ELLIPSE('',#6445,1.08239220029239,1.);
#149=ELLIPSE('',#6447,1.08239220029239,1.);
#150=ELLIPSE('',#6449,1.08239220029239,1.);
#151=ELLIPSE('',#6451,1.08239220029239,1.);
#152=ELLIPSE('',#6453,1.08239220029239,1.);
#153=ELLIPSE('',#6455,1.0823922002924,1.);
#154=ELLIPSE('',#6457,1.08239220029239,1.);
#155=ELLIPSE('',#6459,1.08239220029239,1.);
#156=ELLIPSE('',#6461,1.0823922002924,1.);
#157=ELLIPSE('',#6463,1.0823922002924,1.);
#158=ELLIPSE('',#6465,1.08239220029239,1.);
#222=SHAPE_REPRESENTATION_RELATIONSHIP('SRR','None',#10176,#232);
#232=ADVANCED_BREP_SHAPE_REPRESENTATION('',(#252),#10128);
#242=STYLED_ITEM('',(#10247),#252);
#252=MANIFOLD_SOLID_BREP('Middle_Block_01',#5886);
#308=FACE_BOUND('',#1119,.T.);
#309=FACE_BOUND('',#1120,.T.);
#310=FACE_BOUND('',#1121,.T.);
#311=FACE_BOUND('',#1122,.T.);
#312=FACE_BOUND('',#1138,.T.);
#313=FACE_BOUND('',#1139,.T.);
#314=FACE_BOUND('',#1140,.T.);
#315=FACE_BOUND('',#1141,.T.);
#425=PLANE('',#6436);
#426=PLANE('',#6437);
#427=PLANE('',#6438);
#428=PLANE('',#6439);
#429=PLANE('',#6440);
#430=PLANE('',#6441);
#431=PLANE('',#6442);
#432=PLANE('',#6467);
#433=PLANE('',#6468);
#434=PLANE('',#6469);
#435=PLANE('',#6470);
#436=PLANE('',#6471);
#437=PLANE('',#6472);
#438=PLANE('',#6473);
#694=FACE_OUTER_BOUND('',#1096,.T.);
#695=FACE_OUTER_BOUND('',#1097,.T.);
#696=FACE_OUTER_BOUND('',#1098,.T.);
#697=FACE_OUTER_BOUND('',#1099,.T.);
#698=FACE_OUTER_BOUND('',#1100,.T.);
#699=FACE_OUTER_BOUND('',#1101,.T.);
#700=FACE_OUTER_BOUND('',#1102,.T.);
#701=FACE_OUTER_BOUND('',#1103,.T.);
#702=FACE_OUTER_BOUND('',#1104,.T.);
#703=FACE_OUTER_BOUND('',#1105,.T.);
#704=FACE_OUTER_BOUND('',#1106,.T.);
#705=FACE_OUTER_BOUND('',#1107,.T.);
#706=FACE_OUTER_BOUND('',#1108,.T.);
#707=FACE_OUTER_BOUND('',#1109,.T.);
#708=FACE_OUTER_BOUND('',#1110,.T.);
#709=FACE_OUTER_BOUND('',#1111,.T.);
#710=FACE_OUTER_BOUND('',#1112,.T.);
#711=FACE_OUTER_BOUND('',#1113,.T.);
#712=FACE_OUTER_BOUND('',#1114,.T.);
#713=FACE_OUTER_BOUND('',#1115,.T.);
#714=FACE_OUTER_BOUND('',#1116,.T.);
#715=FACE_OUTER_BOUND('',#1117,.T.);
#716=FACE_OUTER_BOUND('',#1118,.T.);
#717=FACE_OUTER_BOUND('',#1123,.T.);
#718=FACE_OUTER_BOUND('',#1124,.T.);
#719=FACE_OUTER_BOUND('',#1125,.T.);
#720=FACE_OUTER_BOUND('',#1126,.T.);
#721=FACE_OUTER_BOUND('',#1127,.T.);
#722=FACE_OUTER_BOUND('',#1128,.T.);
#723=FACE_OUTER_BOUND('',#1129,.T.);
#724=FACE_OUTER_BOUND('',#1130,.T.);
#725=FACE_OUTER_BOUND('',#1131,.T.);
#726=FACE_OUTER_BOUND('',#1132,.T.);
#727=FACE_OUTER_BOUND('',#1133,.T.);
#728=FACE_OUTER_BOUND('',#1134,.T.);
#729=FACE_OUTER_BOUND('',#1135,.T.);
#730=FACE_OUTER_BOUND('',#1136,.T.);
#731=FACE_OUTER_BOUND('',#1137,.T.);
#732=FACE_OUTER_BOUND('',#1142,.T.);
#733=FACE_OUTER_BOUND('',#1143,.T.);
#734=FACE_OUTER_BOUND('',#1144,.T.);
#735=FACE_OUTER_BOUND('',#1145,.T.);
#1096=EDGE_LOOP('',(#4776,#4777,#4778,#4779));
#1097=EDGE_LOOP('',(#4780,#4781,#4782,#4783));
#1098=EDGE_LOOP('',(#4784,#4785,#4786,#4787));
#1099=EDGE_LOOP('',(#4788,#4789,#4790,#4791));
#1100=EDGE_LOOP('',(#4792,#4793,#4794,#4795));
#1101=EDGE_LOOP('',(#4796,#4797,#4798,#4799));
#1102=EDGE_LOOP('',(#4800,#4801,#4802,#4803));
#1103=EDGE_LOOP('',(#4804,#4805,#4806,#4807));
#1104=EDGE_LOOP('',(#4808,#4809,#4810,#4811));
#1105=EDGE_LOOP('',(#4812,#4813,#4814,#4815));
#1106=EDGE_LOOP('',(#4816,#4817,#4818,#4819));
#1107=EDGE_LOOP('',(#4820,#4821,#4822,#4823));
#1108=EDGE_LOOP('',(#4824,#4825,#4826,#4827));
#1109=EDGE_LOOP('',(#4828,#4829,#4830,#4831));
#1110=EDGE_LOOP('',(#4832,#4833,#4834,#4835));
#1111=EDGE_LOOP('',(#4836,#4837,#4838,#4839));
#1112=EDGE_LOOP('',(#4840,#4841,#4842,#4843));
#1113=EDGE_LOOP('',(#4844,#4845,#4846,#4847));
#1114=EDGE_LOOP('',(#4848,#4849,#4850,#4851));
#1115=EDGE_LOOP('',(#4852,#4853,#4854,#4855));
#1116=EDGE_LOOP('',(#4856,#4857,#4858,#4859));
#1117=EDGE_LOOP('',(#4860,#4861,#4862,#4863));
#1118=EDGE_LOOP('',(#4864,#4865,#4866,#4867,#4868,#4869,#4870,#4871,#4872,
#4873,#4874,#4875));
#1119=EDGE_LOOP('',(#4876));
#1120=EDGE_LOOP('',(#4877));
#1121=EDGE_LOOP('',(#4878));
#1122=EDGE_LOOP('',(#4879));
#1123=EDGE_LOOP('',(#4880,#4881,#4882,#4883));
#1124=EDGE_LOOP('',(#4884,#4885,#4886,#4887));
#1125=EDGE_LOOP('',(#4888,#4889,#4890,#4891));
#1126=EDGE_LOOP('',(#4892,#4893,#4894,#4895));
#1127=EDGE_LOOP('',(#4896,#4897,#4898,#4899));
#1128=EDGE_LOOP('',(#4900,#4901,#4902,#4903));
#1129=EDGE_LOOP('',(#4904,#4905,#4906,#4907));
#1130=EDGE_LOOP('',(#4908,#4909,#4910,#4911));
#1131=EDGE_LOOP('',(#4912,#4913,#4914,#4915));
#1132=EDGE_LOOP('',(#4916,#4917,#4918,#4919));
#1133=EDGE_LOOP('',(#4920,#4921,#4922,#4923));
#1134=EDGE_LOOP('',(#4924,#4925,#4926,#4927));
#1135=EDGE_LOOP('',(#4928,#4929,#4930,#4931));
#1136=EDGE_LOOP('',(#4932,#4933,#4934,#4935));
#1137=EDGE_LOOP('',(#4936,#4937,#4938,#4939,#4940,#4941,#4942,#4943,#4944,
#4945,#4946,#4947));
#1138=EDGE_LOOP('',(#4948));
#1139=EDGE_LOOP('',(#4949));
#1140=EDGE_LOOP('',(#4950));
#1141=EDGE_LOOP('',(#4951));
#1142=EDGE_LOOP('',(#4952,#4953,#4954,#4955));
#1143=EDGE_LOOP('',(#4956,#4957,#4958,#4959));
#1144=EDGE_LOOP('',(#4960,#4961,#4962,#4963));
#1145=EDGE_LOOP('',(#4964,#4965,#4966,#4967));
#1596=LINE('',#9542,#2146);
#1597=LINE('',#9548,#2147);
#1598=LINE('',#9554,#2148);
#1599=LINE('',#9560,#2149);
#1600=LINE('',#9565,#2150);
#1601=LINE('',#9569,#2151);
#1602=LINE('',#9574,#2152);
#1603=LINE('',#9578,#2153);
#1604=LINE('',#9582,#2154);
#1605=LINE('',#9585,#2155);
#1606=LINE('',#9589,#2156);
#1607=LINE('',#9593,#2157);
#1608=LINE('',#9597,#2158);
#1609=LINE('',#9600,#2159);
#1610=LINE('',#9602,#2160);
#1611=LINE('',#9603,#2161);
#1612=LINE('',#9606,#2162);
#1613=LINE('',#9608,#2163);
#1614=LINE('',#9612,#2164);
#1615=LINE('',#9614,#2165);
#1616=LINE('',#9617,#2166);
#1617=LINE('',#9618,#2167);
#1618=LINE('',#9621,#2168);
#1619=LINE('',#9623,#2169);
#1620=LINE('',#9627,#2170);
#1621=LINE('',#9629,#2171);
#1622=LINE('',#9632,#2172);
#1623=LINE('',#9633,#2173);
#1624=LINE('',#9636,#2174);
#1625=LINE('',#9638,#2175);
#1626=LINE('',#9639,#2176);
#1627=LINE('',#9642,#2177);
#1628=LINE('',#9643,#2178);
#1629=LINE('',#9646,#2179);
#1630=LINE('',#9647,#2180);
#1631=LINE('',#9650,#2181);
#1632=LINE('',#9651,#2182);
#1633=LINE('',#9654,#2183);
#1634=LINE('',#9655,#2184);
#1635=LINE('',#9658,#2185);
#1636=LINE('',#9659,#2186);
#1637=LINE('',#9664,#2187);
#1638=LINE('',#9668,#2188);
#1639=LINE('',#9672,#2189);
#1640=LINE('',#9675,#2190);
#1641=LINE('',#9678,#2191);
#1642=LINE('',#9681,#2192);
#1643=LINE('',#9684,#2193);
#1644=LINE('',#9687,#2194);
#1645=LINE('',#9690,#2195);
#1646=LINE('',#9692,#2196);
#1647=LINE('',#9695,#2197);
#1648=LINE('',#9699,#2198);
#1649=LINE('',#9703,#2199);
#1650=LINE('',#9707,#2200);
#1651=LINE('',#9711,#2201);
#1652=LINE('',#9715,#2202);
#1653=LINE('',#9718,#2203);
#1654=LINE('',#9719,#2204);
#1655=LINE('',#9721,#2205);
#1656=LINE('',#9723,#2206);
#1657=LINE('',#9726,#2207);
#1658=LINE('',#9728,#2208);
#1659=LINE('',#9730,#2209);
#2146=VECTOR('',#7788,3.);
#2147=VECTOR('',#7795,3.);
#2148=VECTOR('',#7802,3.);
#2149=VECTOR('',#7809,3.);
#2150=VECTOR('',#7814,10.);
#2151=VECTOR('',#7817,10.);
#2152=VECTOR('',#7822,10.);
#2153=VECTOR('',#7825,10.);
#2154=VECTOR('',#7830,10.);
#2155=VECTOR('',#7833,10.);
#2156=VECTOR('',#7836,10.);
#2157=VECTOR('',#7839,10.);
#2158=VECTOR('',#7844,10.);
#2159=VECTOR('',#7847,10.);
#2160=VECTOR('',#7850,10.);
#2161=VECTOR('',#7851,10.);
#2162=VECTOR('',#7854,10.);
#2163=VECTOR('',#7855,10.);
#2164=VECTOR('',#7860,10.);
#2165=VECTOR('',#7861,10.);
#2166=VECTOR('',#7866,10.);
#2167=VECTOR('',#7867,10.);
#2168=VECTOR('',#7870,10.);
#2169=VECTOR('',#7871,10.);
#2170=VECTOR('',#7876,10.);
#2171=VECTOR('',#7877,10.);
#2172=VECTOR('',#7882,10.);
#2173=VECTOR('',#7883,10.);
#2174=VECTOR('',#7886,10.);
#2175=VECTOR('',#7887,10.);
#2176=VECTOR('',#7888,10.);
#2177=VECTOR('',#7891,10.);
#2178=VECTOR('',#7892,10.);
#2179=VECTOR('',#7895,10.);
#2180=VECTOR('',#7896,10.);
#2181=VECTOR('',#7899,10.);
#2182=VECTOR('',#7900,10.);
#2183=VECTOR('',#7903,10.);
#2184=VECTOR('',#7904,10.);
#2185=VECTOR('',#7907,10.);
#2186=VECTOR('',#7908,10.);
#2187=VECTOR('',#7913,10.);
#2188=VECTOR('',#7916,10.);
#2189=VECTOR('',#7921,10.);
#2190=VECTOR('',#7924,10.);
#2191=VECTOR('',#7927,10.);
#2192=VECTOR('',#7930,10.);
#2193=VECTOR('',#7933,10.);
#2194=VECTOR('',#7936,10.);
#2195=VECTOR('',#7939,10.);
#2196=VECTOR('',#7942,10.);
#2197=VECTOR('',#7945,10.);
#2198=VECTOR('',#7950,10.);
#2199=VECTOR('',#7955,10.);
#2200=VECTOR('',#7960,10.);
#2201=VECTOR('',#7965,10.);
#2202=VECTOR('',#7970,10.);
#2203=VECTOR('',#7975,10.);
#2204=VECTOR('',#7976,10.);
#2205=VECTOR('',#7979,10.);
#2206=VECTOR('',#7982,10.);
#2207=VECTOR('',#7987,10.);
#2208=VECTOR('',#7990,10.);
#2209=VECTOR('',#7993,10.);
#2414=CIRCLE('',#6401,3.);
#2415=CIRCLE('',#6402,3.);
#2416=CIRCLE('',#6404,3.);
#2417=CIRCLE('',#6405,3.);
#2418=CIRCLE('',#6407,3.);
#2419=CIRCLE('',#6408,3.);
#2420=CIRCLE('',#6410,3.);
#2421=CIRCLE('',#6411,3.);
#2750=VERTEX_POINT('',#9539);
#2751=VERTEX_POINT('',#9541);
#2752=VERTEX_POINT('',#9545);
#2753=VERTEX_POINT('',#9547);
#2754=VERTEX_POINT('',#9551);
#2755=VERTEX_POINT('',#9553);
#2756=VERTEX_POINT('',#9557);
#2757=VERTEX_POINT('',#9559);
#2758=VERTEX_POINT('',#9563);
#2759=VERTEX_POINT('',#9564);
#2760=VERTEX_POINT('',#9566);
#2761=VERTEX_POINT('',#9568);
#2762=VERTEX_POINT('',#9572);
#2763=VERTEX_POINT('',#9573);
#2764=VERTEX_POINT('',#9575);
#2765=VERTEX_POINT('',#9577);
#2766=VERTEX_POINT('',#9581);
#2767=VERTEX_POINT('',#9583);
#2768=VERTEX_POINT('',#9587);
#2769=VERTEX_POINT('',#9588);
#2770=VERTEX_POINT('',#9590);
#2771=VERTEX_POINT('',#9592);
#2772=VERTEX_POINT('',#9596);
#2773=VERTEX_POINT('',#9598);
#2774=VERTEX_POINT('',#9605);
#2775=VERTEX_POINT('',#9607);
#2776=VERTEX_POINT('',#9611);
#2777=VERTEX_POINT('',#9613);
#2778=VERTEX_POINT('',#9620);
#2779=VERTEX_POINT('',#9622);
#2780=VERTEX_POINT('',#9626);
#2781=VERTEX_POINT('',#9628);
#2782=VERTEX_POINT('',#9635);
#2783=VERTEX_POINT('',#9637);
#2784=VERTEX_POINT('',#9641);
#2785=VERTEX_POINT('',#9645);
#2786=VERTEX_POINT('',#9649);
#2787=VERTEX_POINT('',#9653);
#2788=VERTEX_POINT('',#9657);
#2789=VERTEX_POINT('',#9662);
#2790=VERTEX_POINT('',#9663);
#2791=VERTEX_POINT('',#9665);
#2792=VERTEX_POINT('',#9667);
#2793=VERTEX_POINT('',#9671);
#2794=VERTEX_POINT('',#9673);
#2795=VERTEX_POINT('',#9677);
#2796=VERTEX_POINT('',#9679);
#2797=VERTEX_POINT('',#9683);
#2798=VERTEX_POINT('',#9685);
#2799=VERTEX_POINT('',#9689);
#2800=VERTEX_POINT('',#9694);
#2801=VERTEX_POINT('',#9698);
#2802=VERTEX_POINT('',#9702);
#2803=VERTEX_POINT('',#9706);
#2804=VERTEX_POINT('',#9710);
#2805=VERTEX_POINT('',#9714);
#3440=EDGE_CURVE('',#2750,#2750,#2414,.T.);
#3441=EDGE_CURVE('',#2750,#2751,#1596,.T.);
#3442=EDGE_CURVE('',#2751,#2751,#2415,.T.);
#3443=EDGE_CURVE('',#2752,#2752,#2416,.T.);
#3444=EDGE_CURVE('',#2752,#2753,#1597,.T.);
#3445=EDGE_CURVE('',#2753,#2753,#2417,.T.);
#3446=EDGE_CURVE('',#2754,#2754,#2418,.T.);
#3447=EDGE_CURVE('',#2754,#2755,#1598,.T.);
#3448=EDGE_CURVE('',#2755,#2755,#2419,.T.);
#3449=EDGE_CURVE('',#2756,#2756,#2420,.T.);
#3450=EDGE_CURVE('',#2756,#2757,#1599,.T.);
#3451=EDGE_CURVE('',#2757,#2757,#2421,.T.);
#3452=EDGE_CURVE('',#2758,#2759,#1600,.T.);
#3453=EDGE_CURVE('',#2759,#2760,#135,.T.);
#3454=EDGE_CURVE('',#2760,#2761,#1601,.T.);
#3455=EDGE_CURVE('',#2758,#2761,#136,.T.);
#3456=EDGE_CURVE('',#2762,#2763,#1602,.T.);
#3457=EDGE_CURVE('',#2763,#2764,#137,.T.);
#3458=EDGE_CURVE('',#2764,#2765,#1603,.T.);
#3459=EDGE_CURVE('',#2765,#2762,#138,.T.);
#3460=EDGE_CURVE('',#2763,#2766,#1604,.T.);
#3461=EDGE_CURVE('',#2766,#2767,#139,.T.);
#3462=EDGE_CURVE('',#2767,#2764,#1605,.T.);
#3463=EDGE_CURVE('',#2768,#2769,#1606,.T.);
#3464=EDGE_CURVE('',#2769,#2770,#140,.T.);
#3465=EDGE_CURVE('',#2770,#2771,#1607,.T.);
#3466=EDGE_CURVE('',#2771,#2768,#141,.T.);
#3467=EDGE_CURVE('',#2766,#2772,#1608,.T.);
#3468=EDGE_CURVE('',#2772,#2773,#142,.T.);
#3469=EDGE_CURVE('',#2773,#2767,#1609,.T.);
#3470=EDGE_CURVE('',#2769,#2773,#1610,.T.);
#3471=EDGE_CURVE('',#2772,#2770,#1611,.T.);
#3472=EDGE_CURVE('',#2774,#2768,#1612,.T.);
#3473=EDGE_CURVE('',#2771,#2775,#1613,.T.);
#3474=EDGE_CURVE('',#2775,#2774,#143,.T.);
#3475=EDGE_CURVE('',#2776,#2774,#1614,.T.);
#3476=EDGE_CURVE('',#2775,#2777,#1615,.T.);
#3477=EDGE_CURVE('',#2777,#2776,#144,.T.);
#3478=EDGE_CURVE('',#2759,#2762,#1616,.T.);
#3479=EDGE_CURVE('',#2765,#2760,#1617,.T.);
#3480=EDGE_CURVE('',#2778,#2776,#1618,.T.);
#3481=EDGE_CURVE('',#2777,#2779,#1619,.T.);
#3482=EDGE_CURVE('',#2779,#2778,#145,.T.);
#3483=EDGE_CURVE('',#2780,#2778,#1620,.T.);
#3484=EDGE_CURVE('',#2779,#2781,#1621,.T.);
#3485=EDGE_CURVE('',#2781,#2780,#146,.T.);
#3486=EDGE_CURVE('',#2761,#2780,#1622,.T.);
#3487=EDGE_CURVE('',#2781,#2758,#1623,.T.);
#3488=EDGE_CURVE('',#2765,#2782,#1624,.T.);
#3489=EDGE_CURVE('',#2783,#2782,#1625,.T.);
#3490=EDGE_CURVE('',#2783,#2760,#1626,.T.);
#3491=EDGE_CURVE('',#2764,#2784,#1627,.T.);
#3492=EDGE_CURVE('',#2782,#2784,#1628,.T.);
#3493=EDGE_CURVE('',#2767,#2785,#1629,.T.);
#3494=EDGE_CURVE('',#2784,#2785,#1630,.T.);
#3495=EDGE_CURVE('',#2786,#2773,#1631,.T.);
#3496=EDGE_CURVE('',#2785,#2786,#1632,.T.);
#3497=EDGE_CURVE('',#2769,#2787,#1633,.T.);
#3498=EDGE_CURVE('',#2786,#2787,#1634,.T.);
#3499=EDGE_CURVE('',#2768,#2788,#1635,.T.);
#3500=EDGE_CURVE('',#2787,#2788,#1636,.T.);
#3501=EDGE_CURVE('',#2789,#2790,#1637,.T.);
#3502=EDGE_CURVE('',#2790,#2791,#147,.T.);
#3503=EDGE_CURVE('',#2791,#2792,#1638,.T.);
#3504=EDGE_CURVE('',#2789,#2792,#148,.T.);
#3505=EDGE_CURVE('',#2790,#2793,#1639,.T.);
#3506=EDGE_CURVE('',#2793,#2794,#149,.T.);
#3507=EDGE_CURVE('',#2794,#2791,#1640,.T.);
#3508=EDGE_CURVE('',#2793,#2795,#1641,.T.);
#3509=EDGE_CURVE('',#2795,#2796,#150,.T.);
#3510=EDGE_CURVE('',#2796,#2794,#1642,.T.);
#3511=EDGE_CURVE('',#2795,#2797,#1643,.T.);
#3512=EDGE_CURVE('',#2797,#2798,#151,.T.);
#3513=EDGE_CURVE('',#2798,#2796,#1644,.T.);
#3514=EDGE_CURVE('',#2797,#2799,#1645,.T.);
#3515=EDGE_CURVE('',#2799,#2788,#152,.T.);
#3516=EDGE_CURVE('',#2788,#2798,#1646,.T.);
#3517=EDGE_CURVE('',#2799,#2800,#1647,.T.);
#3518=EDGE_CURVE('',#2800,#2787,#153,.T.);
#3519=EDGE_CURVE('',#2800,#2801,#1648,.T.);
#3520=EDGE_CURVE('',#2801,#2786,#154,.T.);
#3521=EDGE_CURVE('',#2801,#2802,#1649,.T.);
#3522=EDGE_CURVE('',#2802,#2785,#155,.T.);
#3523=EDGE_CURVE('',#2802,#2803,#1650,.T.);
#3524=EDGE_CURVE('',#2803,#2784,#156,.T.);
#3525=EDGE_CURVE('',#2803,#2804,#1651,.T.);
#3526=EDGE_CURVE('',#2804,#2782,#157,.T.);
#3527=EDGE_CURVE('',#2804,#2805,#1652,.T.);
#3528=EDGE_CURVE('',#2805,#2783,#158,.T.);
#3529=EDGE_CURVE('',#2792,#2783,#1653,.T.);
#3530=EDGE_CURVE('',#2805,#2789,#1654,.T.);
#3531=EDGE_CURVE('',#2761,#2792,#1655,.T.);
#3532=EDGE_CURVE('',#2780,#2791,#1656,.T.);
#3533=EDGE_CURVE('',#2778,#2794,#1657,.T.);
#3534=EDGE_CURVE('',#2776,#2796,#1658,.T.);
#3535=EDGE_CURVE('',#2774,#2798,#1659,.T.);
#4776=ORIENTED_EDGE('',*,*,#3440,.F.);
#4777=ORIENTED_EDGE('',*,*,#3441,.T.);
#4778=ORIENTED_EDGE('',*,*,#3442,.F.);
#4779=ORIENTED_EDGE('',*,*,#3441,.F.);
#4780=ORIENTED_EDGE('',*,*,#3443,.F.);
#4781=ORIENTED_EDGE('',*,*,#3444,.T.);
#4782=ORIENTED_EDGE('',*,*,#3445,.F.);
#4783=ORIENTED_EDGE('',*,*,#3444,.F.);
#4784=ORIENTED_EDGE('',*,*,#3446,.F.);
#4785=ORIENTED_EDGE('',*,*,#3447,.T.);
#4786=ORIENTED_EDGE('',*,*,#3448,.F.);
#4787=ORIENTED_EDGE('',*,*,#3447,.F.);
#4788=ORIENTED_EDGE('',*,*,#3449,.F.);
#4789=ORIENTED_EDGE('',*,*,#3450,.T.);
#4790=ORIENTED_EDGE('',*,*,#3451,.F.);
#4791=ORIENTED_EDGE('',*,*,#3450,.F.);
#4792=ORIENTED_EDGE('',*,*,#3452,.T.);
#4793=ORIENTED_EDGE('',*,*,#3453,.T.);
#4794=ORIENTED_EDGE('',*,*,#3454,.T.);
#4795=ORIENTED_EDGE('',*,*,#3455,.F.);
#4796=ORIENTED_EDGE('',*,*,#3456,.T.);
#4797=ORIENTED_EDGE('',*,*,#3457,.T.);
#4798=ORIENTED_EDGE('',*,*,#3458,.T.);
#4799=ORIENTED_EDGE('',*,*,#3459,.T.);
#4800=ORIENTED_EDGE('',*,*,#3460,.T.);
#4801=ORIENTED_EDGE('',*,*,#3461,.T.);
#4802=ORIENTED_EDGE('',*,*,#3462,.T.);
#4803=ORIENTED_EDGE('',*,*,#3457,.F.);
#4804=ORIENTED_EDGE('',*,*,#3463,.T.);
#4805=ORIENTED_EDGE('',*,*,#3464,.T.);
#4806=ORIENTED_EDGE('',*,*,#3465,.T.);
#4807=ORIENTED_EDGE('',*,*,#3466,.T.);
#4808=ORIENTED_EDGE('',*,*,#3467,.T.);
#4809=ORIENTED_EDGE('',*,*,#3468,.T.);
#4810=ORIENTED_EDGE('',*,*,#3469,.T.);
#4811=ORIENTED_EDGE('',*,*,#3461,.F.);
#4812=ORIENTED_EDGE('',*,*,#3470,.T.);
#4813=ORIENTED_EDGE('',*,*,#3468,.F.);
#4814=ORIENTED_EDGE('',*,*,#3471,.T.);
#4815=ORIENTED_EDGE('',*,*,#3464,.F.);
#4816=ORIENTED_EDGE('',*,*,#3472,.T.);
#4817=ORIENTED_EDGE('',*,*,#3466,.F.);
#4818=ORIENTED_EDGE('',*,*,#3473,.T.);
#4819=ORIENTED_EDGE('',*,*,#3474,.T.);
#4820=ORIENTED_EDGE('',*,*,#3475,.T.);
#4821=ORIENTED_EDGE('',*,*,#3474,.F.);
#4822=ORIENTED_EDGE('',*,*,#3476,.T.);
#4823=ORIENTED_EDGE('',*,*,#3477,.T.);
#4824=ORIENTED_EDGE('',*,*,#3478,.T.);
#4825=ORIENTED_EDGE('',*,*,#3459,.F.);
#4826=ORIENTED_EDGE('',*,*,#3479,.T.);
#4827=ORIENTED_EDGE('',*,*,#3453,.F.);
#4828=ORIENTED_EDGE('',*,*,#3480,.T.);
#4829=ORIENTED_EDGE('',*,*,#3477,.F.);
#4830=ORIENTED_EDGE('',*,*,#3481,.T.);
#4831=ORIENTED_EDGE('',*,*,#3482,.T.);
#4832=ORIENTED_EDGE('',*,*,#3483,.T.);
#4833=ORIENTED_EDGE('',*,*,#3482,.F.);
#4834=ORIENTED_EDGE('',*,*,#3484,.T.);
#4835=ORIENTED_EDGE('',*,*,#3485,.T.);
#4836=ORIENTED_EDGE('',*,*,#3486,.T.);
#4837=ORIENTED_EDGE('',*,*,#3485,.F.);
#4838=ORIENTED_EDGE('',*,*,#3487,.T.);
#4839=ORIENTED_EDGE('',*,*,#3455,.T.);
#4840=ORIENTED_EDGE('',*,*,#3479,.F.);
#4841=ORIENTED_EDGE('',*,*,#3488,.T.);
#4842=ORIENTED_EDGE('',*,*,#3489,.F.);
#4843=ORIENTED_EDGE('',*,*,#3490,.T.);
#4844=ORIENTED_EDGE('',*,*,#3458,.F.);
#4845=ORIENTED_EDGE('',*,*,#3491,.T.);
#4846=ORIENTED_EDGE('',*,*,#3492,.F.);
#4847=ORIENTED_EDGE('',*,*,#3488,.F.);
#4848=ORIENTED_EDGE('',*,*,#3462,.F.);
#4849=ORIENTED_EDGE('',*,*,#3493,.T.);
#4850=ORIENTED_EDGE('',*,*,#3494,.F.);
#4851=ORIENTED_EDGE('',*,*,#3491,.F.);
#4852=ORIENTED_EDGE('',*,*,#3469,.F.);
#4853=ORIENTED_EDGE('',*,*,#3495,.F.);
#4854=ORIENTED_EDGE('',*,*,#3496,.F.);
#4855=ORIENTED_EDGE('',*,*,#3493,.F.);
#4856=ORIENTED_EDGE('',*,*,#3470,.F.);
#4857=ORIENTED_EDGE('',*,*,#3497,.T.);
#4858=ORIENTED_EDGE('',*,*,#3498,.F.);
#4859=ORIENTED_EDGE('',*,*,#3495,.T.);
#4860=ORIENTED_EDGE('',*,*,#3463,.F.);
#4861=ORIENTED_EDGE('',*,*,#3499,.T.);
#4862=ORIENTED_EDGE('',*,*,#3500,.F.);
#4863=ORIENTED_EDGE('',*,*,#3497,.F.);
#4864=ORIENTED_EDGE('',*,*,#3465,.F.);
#4865=ORIENTED_EDGE('',*,*,#3471,.F.);
#4866=ORIENTED_EDGE('',*,*,#3467,.F.);
#4867=ORIENTED_EDGE('',*,*,#3460,.F.);
#4868=ORIENTED_EDGE('',*,*,#3456,.F.);
#4869=ORIENTED_EDGE('',*,*,#3478,.F.);
#4870=ORIENTED_EDGE('',*,*,#3452,.F.);
#4871=ORIENTED_EDGE('',*,*,#3487,.F.);
#4872=ORIENTED_EDGE('',*,*,#3484,.F.);
#4873=ORIENTED_EDGE('',*,*,#3481,.F.);
#4874=ORIENTED_EDGE('',*,*,#3476,.F.);
#4875=ORIENTED_EDGE('',*,*,#3473,.F.);
#4876=ORIENTED_EDGE('',*,*,#3442,.T.);
#4877=ORIENTED_EDGE('',*,*,#3445,.T.);
#4878=ORIENTED_EDGE('',*,*,#3448,.T.);
#4879=ORIENTED_EDGE('',*,*,#3451,.T.);
#4880=ORIENTED_EDGE('',*,*,#3501,.T.);
#4881=ORIENTED_EDGE('',*,*,#3502,.T.);
#4882=ORIENTED_EDGE('',*,*,#3503,.T.);
#4883=ORIENTED_EDGE('',*,*,#3504,.F.);
#4884=ORIENTED_EDGE('',*,*,#3505,.T.);
#4885=ORIENTED_EDGE('',*,*,#3506,.T.);
#4886=ORIENTED_EDGE('',*,*,#3507,.T.);
#4887=ORIENTED_EDGE('',*,*,#3502,.F.);
#4888=ORIENTED_EDGE('',*,*,#3508,.T.);
#4889=ORIENTED_EDGE('',*,*,#3509,.T.);
#4890=ORIENTED_EDGE('',*,*,#3510,.T.);
#4891=ORIENTED_EDGE('',*,*,#3506,.F.);
#4892=ORIENTED_EDGE('',*,*,#3511,.T.);
#4893=ORIENTED_EDGE('',*,*,#3512,.T.);
#4894=ORIENTED_EDGE('',*,*,#3513,.T.);
#4895=ORIENTED_EDGE('',*,*,#3509,.F.);
#4896=ORIENTED_EDGE('',*,*,#3514,.T.);
#4897=ORIENTED_EDGE('',*,*,#3515,.T.);
#4898=ORIENTED_EDGE('',*,*,#3516,.T.);
#4899=ORIENTED_EDGE('',*,*,#3512,.F.);
#4900=ORIENTED_EDGE('',*,*,#3517,.T.);
#4901=ORIENTED_EDGE('',*,*,#3518,.T.);
#4902=ORIENTED_EDGE('',*,*,#3500,.T.);
#4903=ORIENTED_EDGE('',*,*,#3515,.F.);
#4904=ORIENTED_EDGE('',*,*,#3498,.T.);
#4905=ORIENTED_EDGE('',*,*,#3518,.F.);
#4906=ORIENTED_EDGE('',*,*,#3519,.T.);
#4907=ORIENTED_EDGE('',*,*,#3520,.T.);
#4908=ORIENTED_EDGE('',*,*,#3496,.T.);
#4909=ORIENTED_EDGE('',*,*,#3520,.F.);
#4910=ORIENTED_EDGE('',*,*,#3521,.T.);
#4911=ORIENTED_EDGE('',*,*,#3522,.T.);
#4912=ORIENTED_EDGE('',*,*,#3494,.T.);
#4913=ORIENTED_EDGE('',*,*,#3522,.F.);
#4914=ORIENTED_EDGE('',*,*,#3523,.T.);
#4915=ORIENTED_EDGE('',*,*,#3524,.T.);
#4916=ORIENTED_EDGE('',*,*,#3492,.T.);
#4917=ORIENTED_EDGE('',*,*,#3524,.F.);
#4918=ORIENTED_EDGE('',*,*,#3525,.T.);
#4919=ORIENTED_EDGE('',*,*,#3526,.T.);
#4920=ORIENTED_EDGE('',*,*,#3489,.T.);
#4921=ORIENTED_EDGE('',*,*,#3526,.F.);
#4922=ORIENTED_EDGE('',*,*,#3527,.T.);
#4923=ORIENTED_EDGE('',*,*,#3528,.T.);
#4924=ORIENTED_EDGE('',*,*,#3529,.T.);
#4925=ORIENTED_EDGE('',*,*,#3528,.F.);
#4926=ORIENTED_EDGE('',*,*,#3530,.T.);
#4927=ORIENTED_EDGE('',*,*,#3504,.T.);
#4928=ORIENTED_EDGE('',*,*,#3454,.F.);
#4929=ORIENTED_EDGE('',*,*,#3490,.F.);
#4930=ORIENTED_EDGE('',*,*,#3529,.F.);
#4931=ORIENTED_EDGE('',*,*,#3531,.F.);
#4932=ORIENTED_EDGE('',*,*,#3486,.F.);
#4933=ORIENTED_EDGE('',*,*,#3531,.T.);
#4934=ORIENTED_EDGE('',*,*,#3503,.F.);
#4935=ORIENTED_EDGE('',*,*,#3532,.F.);
#4936=ORIENTED_EDGE('',*,*,#3501,.F.);
#4937=ORIENTED_EDGE('',*,*,#3530,.F.);
#4938=ORIENTED_EDGE('',*,*,#3527,.F.);
#4939=ORIENTED_EDGE('',*,*,#3525,.F.);
#4940=ORIENTED_EDGE('',*,*,#3523,.F.);
#4941=ORIENTED_EDGE('',*,*,#3521,.F.);
#4942=ORIENTED_EDGE('',*,*,#3519,.F.);
#4943=ORIENTED_EDGE('',*,*,#3517,.F.);
#4944=ORIENTED_EDGE('',*,*,#3514,.F.);
#4945=ORIENTED_EDGE('',*,*,#3511,.F.);
#4946=ORIENTED_EDGE('',*,*,#3508,.F.);
#4947=ORIENTED_EDGE('',*,*,#3505,.F.);
#4948=ORIENTED_EDGE('',*,*,#3440,.T.);
#4949=ORIENTED_EDGE('',*,*,#3443,.T.);
#4950=ORIENTED_EDGE('',*,*,#3446,.T.);
#4951=ORIENTED_EDGE('',*,*,#3449,.T.);
#4952=ORIENTED_EDGE('',*,*,#3483,.F.);
#4953=ORIENTED_EDGE('',*,*,#3532,.T.);
#4954=ORIENTED_EDGE('',*,*,#3507,.F.);
#4955=ORIENTED_EDGE('',*,*,#3533,.F.);
#4956=ORIENTED_EDGE('',*,*,#3480,.F.);
#4957=ORIENTED_EDGE('',*,*,#3533,.T.);
#4958=ORIENTED_EDGE('',*,*,#3510,.F.);
#4959=ORIENTED_EDGE('',*,*,#3534,.F.);
#4960=ORIENTED_EDGE('',*,*,#3475,.F.);
#4961=ORIENTED_EDGE('',*,*,#3534,.T.);
#4962=ORIENTED_EDGE('',*,*,#3513,.F.);
#4963=ORIENTED_EDGE('',*,*,#3535,.F.);
#4964=ORIENTED_EDGE('',*,*,#3472,.F.);
#4965=ORIENTED_EDGE('',*,*,#3535,.T.);
#4966=ORIENTED_EDGE('',*,*,#3516,.F.);
#4967=ORIENTED_EDGE('',*,*,#3499,.F.);
#5450=CYLINDRICAL_SURFACE('',#6400,3.);
#5451=CYLINDRICAL_SURFACE('',#6403,3.);
#5452=CYLINDRICAL_SURFACE('',#6406,3.);
#5453=CYLINDRICAL_SURFACE('',#6409,3.);
#5454=CYLINDRICAL_SURFACE('',#6412,1.);
#5455=CYLINDRICAL_SURFACE('',#6415,1.);
#5456=CYLINDRICAL_SURFACE('',#6418,1.);
#5457=CYLINDRICAL_SURFACE('',#6420,1.);
#5458=CYLINDRICAL_SURFACE('',#6423,1.);
#5459=CYLINDRICAL_SURFACE('',#6425,1.);
#5460=CYLINDRICAL_SURFACE('',#6426,1.);
#5461=CYLINDRICAL_SURFACE('',#6428,1.);
#5462=CYLINDRICAL_SURFACE('',#6430,1.);
#5463=CYLINDRICAL_SURFACE('',#6431,1.);
#5464=CYLINDRICAL_SURFACE('',#6433,1.);
#5465=CYLINDRICAL_SURFACE('',#6435,1.);
#5466=CYLINDRICAL_SURFACE('',#6443,1.);
#5467=CYLINDRICAL_SURFACE('',#6446,1.);
#5468=CYLINDRICAL_SURFACE('',#6448,1.);
#5469=CYLINDRICAL_SURFACE('',#6450,1.);
#5470=CYLINDRICAL_SURFACE('',#6452,1.);
#5471=CYLINDRICAL_SURFACE('',#6454,1.);
#5472=CYLINDRICAL_SURFACE('',#6456,1.);
#5473=CYLINDRICAL_SURFACE('',#6458,1.);
#5474=CYLINDRICAL_SURFACE('',#6460,1.);
#5475=CYLINDRICAL_SURFACE('',#6462,1.);
#5476=CYLINDRICAL_SURFACE('',#6464,1.);
#5477=CYLINDRICAL_SURFACE('',#6466,1.);
#5757=ADVANCED_FACE('',(#694),#5450,.F.);
#5758=ADVANCED_FACE('',(#695),#5451,.F.);
#5759=ADVANCED_FACE('',(#696),#5452,.F.);
#5760=ADVANCED_FACE('',(#697),#5453,.F.);
#5761=ADVANCED_FACE('',(#698),#5454,.T.);
#5762=ADVANCED_FACE('',(#699),#5455,.T.);
#5763=ADVANCED_FACE('',(#700),#5456,.T.);
#5764=ADVANCED_FACE('',(#701),#5457,.T.);
#5765=ADVANCED_FACE('',(#702),#5458,.T.);
#5766=ADVANCED_FACE('',(#703),#5459,.T.);
#5767=ADVANCED_FACE('',(#704),#5460,.T.);
#5768=ADVANCED_FACE('',(#705),#5461,.T.);
#5769=ADVANCED_FACE('',(#706),#5462,.T.);
#5770=ADVANCED_FACE('',(#707),#5463,.T.);
#5771=ADVANCED_FACE('',(#708),#5464,.T.);
#5772=ADVANCED_FACE('',(#709),#5465,.T.);
#5773=ADVANCED_FACE('',(#710),#425,.T.);
#5774=ADVANCED_FACE('',(#711),#426,.T.);
#5775=ADVANCED_FACE('',(#712),#427,.T.);
#5776=ADVANCED_FACE('',(#713),#428,.T.);
#5777=ADVANCED_FACE('',(#714),#429,.T.);
#5778=ADVANCED_FACE('',(#715),#430,.T.);
#5779=ADVANCED_FACE('',(#716,#308,#309,#310,#311),#431,.F.);
#5780=ADVANCED_FACE('',(#717),#5466,.T.);
#5781=ADVANCED_FACE('',(#718),#5467,.T.);
#5782=ADVANCED_FACE('',(#719),#5468,.T.);
#5783=ADVANCED_FACE('',(#720),#5469,.T.);
#5784=ADVANCED_FACE('',(#721),#5470,.T.);
#5785=ADVANCED_FACE('',(#722),#5471,.T.);
#5786=ADVANCED_FACE('',(#723),#5472,.T.);
#5787=ADVANCED_FACE('',(#724),#5473,.T.);
#5788=ADVANCED_FACE('',(#725),#5474,.T.);
#5789=ADVANCED_FACE('',(#726),#5475,.T.);
#5790=ADVANCED_FACE('',(#727),#5476,.T.);
#5791=ADVANCED_FACE('',(#728),#5477,.T.);
#5792=ADVANCED_FACE('',(#729),#432,.T.);
#5793=ADVANCED_FACE('',(#730),#433,.T.);
#5794=ADVANCED_FACE('',(#731,#312,#313,#314,#315),#434,.T.);
#5795=ADVANCED_FACE('',(#732),#435,.T.);
#5796=ADVANCED_FACE('',(#733),#436,.T.);
#5797=ADVANCED_FACE('',(#734),#437,.T.);
#5798=ADVANCED_FACE('',(#735),#438,.T.);
#5886=CLOSED_SHELL('',(#5757,#5758,#5759,#5760,#5761,#5762,#5763,#5764,
#5765,#5766,#5767,#5768,#5769,#5770,#5771,#5772,#5773,#5774,#5775,#5776,
#5777,#5778,#5779,#5780,#5781,#5782,#5783,#5784,#5785,#5786,#5787,#5788,
#5789,#5790,#5791,#5792,#5793,#5794,#5795,#5796,#5797,#5798));
#6399=AXIS2_PLACEMENT_3D('',#9537,#7782,#7783);
#6400=AXIS2_PLACEMENT_3D('',#9538,#7784,#7785);
#6401=AXIS2_PLACEMENT_3D('',#9540,#7786,#7787);
#6402=AXIS2_PLACEMENT_3D('',#9543,#7789,#7790);
#6403=AXIS2_PLACEMENT_3D('',#9544,#7791,#7792);
#6404=AXIS2_PLACEMENT_3D('',#9546,#7793,#7794);
#6405=AXIS2_PLACEMENT_3D('',#9549,#7796,#7797);
#6406=AXIS2_PLACEMENT_3D('',#9550,#7798,#7799);
#6407=AXIS2_PLACEMENT_3D('',#9552,#7800,#7801);
#6408=AXIS2_PLACEMENT_3D('',#9555,#7803,#7804);
#6409=AXIS2_PLACEMENT_3D('',#9556,#7805,#7806);
#6410=AXIS2_PLACEMENT_3D('',#9558,#7807,#7808);
#6411=AXIS2_PLACEMENT_3D('',#9561,#7810,#7811);
#6412=AXIS2_PLACEMENT_3D('',#9562,#7812,#7813);
#6413=AXIS2_PLACEMENT_3D('',#9567,#7815,#7816);
#6414=AXIS2_PLACEMENT_3D('',#9570,#7818,#7819);
#6415=AXIS2_PLACEMENT_3D('',#9571,#7820,#7821);
#6416=AXIS2_PLACEMENT_3D('',#9576,#7823,#7824);
#6417=AXIS2_PLACEMENT_3D('',#9579,#7826,#7827);
#6418=AXIS2_PLACEMENT_3D('',#9580,#7828,#7829);
#6419=AXIS2_PLACEMENT_3D('',#9584,#7831,#7832);
#6420=AXIS2_PLACEMENT_3D('',#9586,#7834,#7835);
#6421=AXIS2_PLACEMENT_3D('',#9591,#7837,#7838);
#6422=AXIS2_PLACEMENT_3D('',#9594,#7840,#7841);
#6423=AXIS2_PLACEMENT_3D('',#9595,#7842,#7843);
#6424=AXIS2_PLACEMENT_3D('',#9599,#7845,#7846);
#6425=AXIS2_PLACEMENT_3D('',#9601,#7848,#7849);
#6426=AXIS2_PLACEMENT_3D('',#9604,#7852,#7853);
#6427=AXIS2_PLACEMENT_3D('',#9609,#7856,#7857);
#6428=AXIS2_PLACEMENT_3D('',#9610,#7858,#7859);
#6429=AXIS2_PLACEMENT_3D('',#9615,#7862,#7863);
#6430=AXIS2_PLACEMENT_3D('',#9616,#7864,#7865);
#6431=AXIS2_PLACEMENT_3D('',#9619,#7868,#7869);
#6432=AXIS2_PLACEMENT_3D('',#9624,#7872,#7873);
#6433=AXIS2_PLACEMENT_3D('',#9625,#7874,#7875);
#6434=AXIS2_PLACEMENT_3D('',#9630,#7878,#7879);
#6435=AXIS2_PLACEMENT_3D('',#9631,#7880,#7881);
#6436=AXIS2_PLACEMENT_3D('',#9634,#7884,#7885);
#6437=AXIS2_PLACEMENT_3D('',#9640,#7889,#7890);
#6438=AXIS2_PLACEMENT_3D('',#9644,#7893,#7894);
#6439=AXIS2_PLACEMENT_3D('',#9648,#7897,#7898);
#6440=AXIS2_PLACEMENT_3D('',#9652,#7901,#7902);
#6441=AXIS2_PLACEMENT_3D('',#9656,#7905,#7906);
#6442=AXIS2_PLACEMENT_3D('',#9660,#7909,#7910);
#6443=AXIS2_PLACEMENT_3D('',#9661,#7911,#7912);
#6444=AXIS2_PLACEMENT_3D('',#9666,#7914,#7915);
#6445=AXIS2_PLACEMENT_3D('',#9669,#7917,#7918);
#6446=AXIS2_PLACEMENT_3D('',#9670,#7919,#7920);
#6447=AXIS2_PLACEMENT_3D('',#9674,#7922,#7923);
#6448=AXIS2_PLACEMENT_3D('',#9676,#7925,#7926);
#6449=AXIS2_PLACEMENT_3D('',#9680,#7928,#7929);
#6450=AXIS2_PLACEMENT_3D('',#9682,#7931,#7932);
#6451=AXIS2_PLACEMENT_3D('',#9686,#7934,#7935);
#6452=AXIS2_PLACEMENT_3D('',#9688,#7937,#7938);
#6453=AXIS2_PLACEMENT_3D('',#9691,#7940,#7941);
#6454=AXIS2_PLACEMENT_3D('',#9693,#7943,#7944);
#6455=AXIS2_PLACEMENT_3D('',#9696,#7946,#7947);
#6456=AXIS2_PLACEMENT_3D('',#9697,#7948,#7949);
#6457=AXIS2_PLACEMENT_3D('',#9700,#7951,#7952);
#6458=AXIS2_PLACEMENT_3D('',#9701,#7953,#7954);
#6459=AXIS2_PLACEMENT_3D('',#9704,#7956,#7957);
#6460=AXIS2_PLACEMENT_3D('',#9705,#7958,#7959);
#6461=AXIS2_PLACEMENT_3D('',#9708,#7961,#7962);
#6462=AXIS2_PLACEMENT_3D('',#9709,#7963,#7964);
#6463=AXIS2_PLACEMENT_3D('',#9712,#7966,#7967);
#6464=AXIS2_PLACEMENT_3D('',#9713,#7968,#7969);
#6465=AXIS2_PLACEMENT_3D('',#9716,#7971,#7972);
#6466=AXIS2_PLACEMENT_3D('',#9717,#7973,#7974);
#6467=AXIS2_PLACEMENT_3D('',#9720,#7977,#7978);
#6468=AXIS2_PLACEMENT_3D('',#9722,#7980,#7981);
#6469=AXIS2_PLACEMENT_3D('',#9724,#7983,#7984);
#6470=AXIS2_PLACEMENT_3D('',#9725,#7985,#7986);
#6471=AXIS2_PLACEMENT_3D('',#9727,#7988,#7989);
#6472=AXIS2_PLACEMENT_3D('',#9729,#7991,#7992);
#6473=AXIS2_PLACEMENT_3D('',#9731,#7994,#7995);
#7782=DIRECTION('axis',(0.,0.,1.));
#7783=DIRECTION('refdir',(1.,0.,0.));
#7784=DIRECTION('center_axis',(0.,0.,-1.));
#7785=DIRECTION('ref_axis',(-1.,0.,0.));
#7786=DIRECTION('center_axis',(0.,0.,-1.));
#7787=DIRECTION('ref_axis',(-1.,0.,0.));
#7788=DIRECTION('',(0.,0.,-1.));
#7789=DIRECTION('center_axis',(0.,0.,1.));
#7790=DIRECTION('ref_axis',(-1.,0.,0.));
#7791=DIRECTION('center_axis',(0.,0.,-1.));
#7792=DIRECTION('ref_axis',(-1.,0.,0.));
#7793=DIRECTION('center_axis',(0.,0.,-1.));
#7794=DIRECTION('ref_axis',(-1.,0.,0.));
#7795=DIRECTION('',(0.,0.,-1.));
#7796=DIRECTION('center_axis',(0.,0.,1.));
#7797=DIRECTION('ref_axis',(-1.,0.,0.));
#7798=DIRECTION('center_axis',(0.,0.,-1.));
#7799=DIRECTION('ref_axis',(-1.,0.,0.));
#7800=DIRECTION('center_axis',(0.,0.,-1.));
#7801=DIRECTION('ref_axis',(-1.,0.,0.));
#7802=DIRECTION('',(0.,0.,-1.));
#7803=DIRECTION('center_axis',(0.,0.,1.));
#7804=DIRECTION('ref_axis',(-1.,0.,0.));
#7805=DIRECTION('center_axis',(0.,0.,-1.));
#7806=DIRECTION('ref_axis',(-1.,0.,0.));
#7807=DIRECTION('center_axis',(0.,0.,-1.));
#7808=DIRECTION('ref_axis',(-1.,0.,0.));
#7809=DIRECTION('',(0.,0.,-1.));
#7810=DIRECTION('center_axis',(0.,0.,1.));
#7811=DIRECTION('ref_axis',(-1.,0.,0.));
#7812=DIRECTION('center_axis',(-1.,0.,0.));
#7813=DIRECTION('ref_axis',(0.,-0.707106781186548,-0.707106781186548));
#7814=DIRECTION('',(1.,0.,0.));
#7815=DIRECTION('center_axis',(-0.923879532511283,-0.382683432365099,4.10284931589583E-15));
#7816=DIRECTION('ref_axis',(0.382683432365098,-0.923879532511283,9.90515446280861E-15));
#7817=DIRECTION('',(-1.,0.,0.));
#7818=DIRECTION('center_axis',(-0.923879532511286,0.382683432365092,0.));
#7819=DIRECTION('ref_axis',(0.382683432365091,0.923879532511286,0.));
#7820=DIRECTION('center_axis',(0.,1.,0.));
#7821=DIRECTION('ref_axis',(0.707106781186551,0.,-0.707106781186544));
#7822=DIRECTION('',(0.,1.,0.));
#7823=DIRECTION('center_axis',(-0.382683432365083,-0.92387953251129,0.));
#7824=DIRECTION('ref_axis',(0.923879532511289,-0.382683432365083,0.));
#7825=DIRECTION('',(0.,-1.,0.));
#7826=DIRECTION('center_axis',(0.382683432365097,0.923879532511284,8.49727915508632E-16));
#7827=DIRECTION('ref_axis',(0.923879532511284,-0.382683432365097,2.05142465794791E-15));
#7828=DIRECTION('center_axis',(0.707106781186548,0.707106781186548,0.));
#7829=DIRECTION('ref_axis',(0.499999999999996,-0.500000000000002,-0.707106781186549));
#7830=DIRECTION('',(0.707106781186548,0.707106781186548,0.));
#7831=DIRECTION('center_axis',(-0.92387953251129,-0.382683432365082,0.));
#7832=DIRECTION('ref_axis',(0.382683432365082,-0.92387953251129,0.));
#7833=DIRECTION('',(-0.707106781186548,-0.707106781186548,0.));
#7834=DIRECTION('center_axis',(0.,1.,0.));
#7835=DIRECTION('ref_axis',(0.707106781186548,0.,-0.707106781186548));
#7836=DIRECTION('',(0.,-1.,0.));
#7837=DIRECTION('center_axis',(0.382683432365093,0.923879532511285,0.));
#7838=DIRECTION('ref_axis',(0.923879532511285,-0.382683432365093,0.));
#7839=DIRECTION('',(0.,1.,0.));
#7840=DIRECTION('center_axis',(0.382683432365092,-0.923879532511286,0.));
#7841=DIRECTION('ref_axis',(-0.923879532511286,-0.382683432365092,0.));
#7842=DIRECTION('center_axis',(1.,4.56509835347174E-16,0.));
#7843=DIRECTION('ref_axis',(0.,-0.707106781186551,-0.707106781186544));
#7844=DIRECTION('',(1.,4.56509835347174E-16,0.));
#7845=DIRECTION('center_axis',(-0.923879532511287,-0.38268343236509,0.));
#7846=DIRECTION('ref_axis',(-0.38268343236509,0.923879532511287,0.));
#7847=DIRECTION('',(-1.,-4.56509835347174E-16,0.));
#7848=DIRECTION('center_axis',(0.707106781186548,0.707106781186547,0.));
#7849=DIRECTION('ref_axis',(0.5,-0.5,-0.707106781186547));
#7850=DIRECTION('',(-0.707106781186548,-0.707106781186547,0.));
#7851=DIRECTION('',(0.707106781186548,0.707106781186547,0.));
#7852=DIRECTION('center_axis',(-0.707106781186548,0.707106781186548,0.));
#7853=DIRECTION('ref_axis',(0.5,0.5,-0.707106781186547));
#7854=DIRECTION('',(0.707106781186548,-0.707106781186548,0.));
#7855=DIRECTION('',(-0.707106781186548,0.707106781186548,0.));
#7856=DIRECTION('center_axis',(0.923879532511286,-0.382683432365092,0.));
#7857=DIRECTION('ref_axis',(-0.382683432365091,-0.923879532511286,0.));
#7858=DIRECTION('center_axis',(-1.,0.,0.));
#7859=DIRECTION('ref_axis',(0.,0.707106781186548,-0.707106781186548));
#7860=DIRECTION('',(1.,0.,0.));
#7861=DIRECTION('',(-1.,0.,0.));
#7862=DIRECTION('center_axis',(0.923879532511286,0.382683432365092,0.));
#7863=DIRECTION('ref_axis',(0.382683432365092,-0.923879532511286,0.));
#7864=DIRECTION('center_axis',(0.707106781186548,0.707106781186548,0.));
#7865=DIRECTION('ref_axis',(0.5,-0.5,-0.707106781186547));
#7866=DIRECTION('',(0.707106781186548,0.707106781186548,0.));
#7867=DIRECTION('',(-0.707106781186548,-0.707106781186548,0.));
#7868=DIRECTION('center_axis',(-0.707106781186548,-0.707106781186548,0.));
#7869=DIRECTION('ref_axis',(-0.5,0.5,-0.707106781186547));
#7870=DIRECTION('',(0.707106781186548,0.707106781186548,0.));
#7871=DIRECTION('',(-0.707106781186548,-0.707106781186548,0.));
#7872=DIRECTION('center_axis',(0.382683432365092,0.923879532511286,0.));
#7873=DIRECTION('ref_axis',(0.923879532511286,-0.382683432365091,0.));
#7874=DIRECTION('center_axis',(0.,-1.,0.));
#7875=DIRECTION('ref_axis',(-0.707106781186548,0.,-0.707106781186548));
#7876=DIRECTION('',(0.,1.,0.));
#7877=DIRECTION('',(0.,-1.,0.));
#7878=DIRECTION('center_axis',(-0.382683432365092,0.923879532511286,0.));
#7879=DIRECTION('ref_axis',(0.923879532511286,0.382683432365092,0.));
#7880=DIRECTION('center_axis',(0.707106781186548,-0.707106781186548,0.));
#7881=DIRECTION('ref_axis',(-0.5,-0.5,-0.707106781186547));
#7882=DIRECTION('',(-0.707106781186548,0.707106781186548,0.));
#7883=DIRECTION('',(0.707106781186548,-0.707106781186548,0.));
#7884=DIRECTION('center_axis',(0.707106781186548,-0.707106781186548,0.));
#7885=DIRECTION('ref_axis',(0.,0.,-1.));
#7886=DIRECTION('',(0.,0.,1.));
#7887=DIRECTION('',(0.707106781186548,0.707106781186548,0.));
#7888=DIRECTION('',(0.,0.,-1.));
#7889=DIRECTION('center_axis',(1.,0.,0.));
#7890=DIRECTION('ref_axis',(0.,1.,0.));
#7891=DIRECTION('',(0.,0.,1.));
#7892=DIRECTION('',(0.,1.,0.));
#7893=DIRECTION('center_axis',(0.707106781186548,-0.707106781186548,0.));
#7894=DIRECTION('ref_axis',(0.707106781186548,0.707106781186548,0.));
#7895=DIRECTION('',(0.,0.,1.));
#7896=DIRECTION('',(0.707106781186548,0.707106781186548,0.));
#7897=DIRECTION('center_axis',(4.56509835347174E-16,-1.,0.));
#7898=DIRECTION('ref_axis',(1.,4.56509835347174E-16,0.));
#7899=DIRECTION('',(0.,0.,-1.));
#7900=DIRECTION('',(1.,4.56509835347174E-16,0.));
#7901=DIRECTION('center_axis',(0.707106781186547,-0.707106781186548,0.));
#7902=DIRECTION('ref_axis',(0.,0.,-1.));
#7903=DIRECTION('',(0.,0.,1.));
#7904=DIRECTION('',(0.707106781186548,0.707106781186547,0.));
#7905=DIRECTION('center_axis',(1.,0.,0.));
#7906=DIRECTION('ref_axis',(0.,1.,0.));
#7907=DIRECTION('',(0.,0.,1.));
#7908=DIRECTION('',(0.,1.,0.));
#7909=DIRECTION('center_axis',(0.,0.,1.));
#7910=DIRECTION('ref_axis',(1.,0.,0.));
#7911=DIRECTION('center_axis',(0.707106781186548,-0.707106781186548,0.));
#7912=DIRECTION('ref_axis',(-0.500000000000005,-0.500000000000005,0.707106781186541));
#7913=DIRECTION('',(-0.707106781186548,0.707106781186548,0.));
#7914=DIRECTION('center_axis',(0.382683432365092,-0.923879532511286,0.));
#7915=DIRECTION('ref_axis',(-0.923879532511286,-0.382683432365092,0.));
#7916=DIRECTION('',(0.707106781186548,-0.707106781186548,0.));
#7917=DIRECTION('center_axis',(0.923879532511286,-0.382683432365092,0.));
#7918=DIRECTION('ref_axis',(-0.382683432365092,-0.923879532511286,0.));
#7919=DIRECTION('center_axis',(0.,-1.,0.));
#7920=DIRECTION('ref_axis',(-0.707106781186554,0.,0.707106781186541));
#7921=DIRECTION('',(0.,1.,0.));
#7922=DIRECTION('center_axis',(-0.382683432365092,-0.923879532511286,0.));
#7923=DIRECTION('ref_axis',(-0.923879532511286,0.382683432365092,0.));
#7924=DIRECTION('',(0.,-1.,0.));
#7925=DIRECTION('center_axis',(-0.707106781186548,-0.707106781186548,0.));
#7926=DIRECTION('ref_axis',(-0.500000000000005,0.500000000000005,0.707106781186541));
#7927=DIRECTION('',(0.707106781186548,0.707106781186548,0.));
#7928=DIRECTION('center_axis',(-0.923879532511286,-0.382683432365092,0.));
#7929=DIRECTION('ref_axis',(-0.382683432365092,0.923879532511286,0.));
#7930=DIRECTION('',(-0.707106781186548,-0.707106781186548,0.));
#7931=DIRECTION('center_axis',(-1.,0.,0.));
#7932=DIRECTION('ref_axis',(0.,0.707106781186554,0.707106781186541));
#7933=DIRECTION('',(1.,0.,0.));
#7934=DIRECTION('center_axis',(-0.923879532511286,0.382683432365092,0.));
#7935=DIRECTION('ref_axis',(0.382683432365092,0.923879532511286,0.));
#7936=DIRECTION('',(-1.,0.,0.));
#7937=DIRECTION('center_axis',(-0.707106781186548,0.707106781186548,0.));
#7938=DIRECTION('ref_axis',(0.500000000000005,0.500000000000005,0.707106781186541));
#7939=DIRECTION('',(0.707106781186548,-0.707106781186548,0.));
#7940=DIRECTION('center_axis',(-0.382683432365092,0.923879532511286,0.));
#7941=DIRECTION('ref_axis',(0.923879532511286,0.382683432365092,0.));
#7942=DIRECTION('',(-0.707106781186548,0.707106781186548,0.));
#7943=DIRECTION('center_axis',(0.,1.,0.));
#7944=DIRECTION('ref_axis',(0.707106781186554,0.,0.707106781186541));
#7945=DIRECTION('',(0.,-1.,0.));
#7946=DIRECTION('center_axis',(0.382683432365093,0.923879532511285,0.));
#7947=DIRECTION('ref_axis',(0.923879532511285,-0.382683432365093,0.));
#7948=DIRECTION('center_axis',(-0.707106781186548,-0.707106781186547,0.));
#7949=DIRECTION('ref_axis',(0.5,-0.5,0.707106781186547));
#7950=DIRECTION('',(-0.707106781186548,-0.707106781186547,0.));
#7951=DIRECTION('center_axis',(0.923879532511287,0.38268343236509,0.));
#7952=DIRECTION('ref_axis',(-0.38268343236509,0.923879532511287,0.));
#7953=DIRECTION('center_axis',(1.,4.56509835347174E-16,0.));
#7954=DIRECTION('ref_axis',(0.,-0.707106781186557,0.707106781186538));
#7955=DIRECTION('',(-1.,-4.56509835347174E-16,0.));
#7956=DIRECTION('center_axis',(0.92387953251129,0.382683432365082,0.));
#7957=DIRECTION('ref_axis',(-0.382683432365082,0.92387953251129,0.));
#7958=DIRECTION('center_axis',(0.707106781186548,0.707106781186548,0.));
#7959=DIRECTION('ref_axis',(0.500000000000005,-0.500000000000005,0.707106781186541));
#7960=DIRECTION('',(-0.707106781186548,-0.707106781186548,0.));
#7961=DIRECTION('center_axis',(0.382683432365087,0.923879532511288,0.));
#7962=DIRECTION('ref_axis',(-0.923879532511288,0.382683432365087,0.));
#7963=DIRECTION('center_axis',(0.,1.,0.));
#7964=DIRECTION('ref_axis',(0.707106781186557,0.,0.707106781186538));
#7965=DIRECTION('',(0.,-1.,0.));
#7966=DIRECTION('center_axis',(0.382683432365097,0.923879532511284,-8.4972791550864E-16));
#7967=DIRECTION('ref_axis',(0.923879532511284,-0.382683432365097,-2.05142465794793E-15));
#7968=DIRECTION('center_axis',(-0.707106781186548,-0.707106781186548,0.));
#7969=DIRECTION('ref_axis',(0.5,-0.5,0.707106781186547));
#7970=DIRECTION('',(-0.707106781186548,-0.707106781186548,0.));
#7971=DIRECTION('center_axis',(0.923879532511283,0.382683432365099,0.));
#7972=DIRECTION('ref_axis',(-0.382683432365099,0.923879532511283,0.));
#7973=DIRECTION('center_axis',(1.,0.,0.));
#7974=DIRECTION('ref_axis',(0.,-0.707106781186554,0.707106781186541));
#7975=DIRECTION('',(1.,0.,0.));
#7976=DIRECTION('',(-1.,0.,0.));
#7977=DIRECTION('center_axis',(0.,-1.,0.));
#7978=DIRECTION('ref_axis',(1.,0.,0.));
#7979=DIRECTION('',(0.,0.,1.));
#7980=DIRECTION('center_axis',(-0.707106781186548,-0.707106781186548,0.));
#7981=DIRECTION('ref_axis',(0.707106781186548,-0.707106781186548,0.));
#7982=DIRECTION('',(0.,0.,1.));
#7983=DIRECTION('center_axis',(0.,0.,1.));
#7984=DIRECTION('ref_axis',(1.,0.,0.));
#7985=DIRECTION('center_axis',(-1.,0.,0.));
#7986=DIRECTION('ref_axis',(0.,-1.,0.));
#7987=DIRECTION('',(0.,0.,1.));
#7988=DIRECTION('center_axis',(-0.707106781186548,0.707106781186548,0.));
#7989=DIRECTION('ref_axis',(-0.707106781186548,-0.707106781186548,0.));
#7990=DIRECTION('',(0.,0.,1.));
#7991=DIRECTION('center_axis',(0.,1.,0.));
#7992=DIRECTION('ref_axis',(-1.,0.,0.));
#7993=DIRECTION('',(0.,0.,1.));
#7994=DIRECTION('center_axis',(0.707106781186548,0.707106781186548,0.));
#7995=DIRECTION('ref_axis',(-0.707106781186548,0.707106781186548,0.));
#9537=CARTESIAN_POINT('',(0.,0.,0.));
#9538=CARTESIAN_POINT('Origin',(-32.4855257306532,-32.7240321735238,86.));
#9539=CARTESIAN_POINT('',(-29.4855257306532,-32.7240321735238,62.));
#9540=CARTESIAN_POINT('Origin',(-32.4855257306532,-32.7240321735238,62.));
#9541=CARTESIAN_POINT('',(-29.4855257306532,-32.7240321735238,50.));
#9542=CARTESIAN_POINT('',(-29.4855257306532,-32.7240321735238,86.));
#9543=CARTESIAN_POINT('Origin',(-32.4855257306532,-32.7240321735238,50.));
#9544=CARTESIAN_POINT('Origin',(32.5144742693468,32.2759678264762,86.));
#9545=CARTESIAN_POINT('',(35.5144742693468,32.2759678264762,62.));
#9546=CARTESIAN_POINT('Origin',(32.5144742693468,32.2759678264762,62.));
#9547=CARTESIAN_POINT('',(35.5144742693468,32.2759678264762,50.));
#9548=CARTESIAN_POINT('',(35.5144742693468,32.2759678264762,86.));
#9549=CARTESIAN_POINT('Origin',(32.5144742693468,32.2759678264762,50.));
#9550=CARTESIAN_POINT('Origin',(-32.4855257306532,32.2759678264762,86.));
#9551=CARTESIAN_POINT('',(-29.4855257306532,32.2759678264762,62.));
#9552=CARTESIAN_POINT('Origin',(-32.4855257306532,32.2759678264762,62.));
#9553=CARTESIAN_POINT('',(-29.4855257306532,32.2759678264762,50.));
#9554=CARTESIAN_POINT('',(-29.4855257306532,32.2759678264762,86.));
#9555=CARTESIAN_POINT('Origin',(-32.4855257306532,32.2759678264762,50.));
#9556=CARTESIAN_POINT('Origin',(32.5144742693468,-7.72403217352376,86.));
#9557=CARTESIAN_POINT('',(35.5144742693468,-7.72403217352376,62.));
#9558=CARTESIAN_POINT('Origin',(32.5144742693468,-7.72403217352376,62.));
#9559=CARTESIAN_POINT('',(35.5144742693468,-7.72403217352376,50.));
#9560=CARTESIAN_POINT('',(35.5144742693468,-7.72403217352376,86.));
#9561=CARTESIAN_POINT('Origin',(32.5144742693468,-7.72403217352376,50.));
#9562=CARTESIAN_POINT('Origin',(-22.5,-49.,51.));
#9563=CARTESIAN_POINT('',(-44.5857864376269,-49.,50.));
#9564=CARTESIAN_POINT('',(15.5857864376269,-49.,50.));
#9565=CARTESIAN_POINT('',(-22.5,-49.,50.));
#9566=CARTESIAN_POINT('',(16.,-50.,51.));
#9567=CARTESIAN_POINT('Origin',(15.5857864376269,-49.,51.));
#9568=CARTESIAN_POINT('',(-45.,-50.,51.));
#9569=CARTESIAN_POINT('',(-22.5,-50.,51.));
#9570=CARTESIAN_POINT('Origin',(-44.5857864376269,-49.,51.));
#9571=CARTESIAN_POINT('Origin',(20.,-25.,51.));
#9572=CARTESIAN_POINT('',(20.,-44.5857864376269,50.));
#9573=CARTESIAN_POINT('',(20.,-30.8578643762691,50.));
#9574=CARTESIAN_POINT('',(20.,-25.,50.));
#9575=CARTESIAN_POINT('',(21.,-31.2720779386421,51.));
#9576=CARTESIAN_POINT('Origin',(20.,-30.8578643762691,51.));
#9577=CARTESIAN_POINT('',(21.,-45.,51.));
#9578=CARTESIAN_POINT('',(21.,-25.,51.));
#9579=CARTESIAN_POINT('Origin',(20.,-44.5857864376269,51.));
#9580=CARTESIAN_POINT('Origin',(22.860912703474,-27.9969516727951,51.));
#9581=CARTESIAN_POINT('',(30.857864376269,-20.,50.));
#9582=CARTESIAN_POINT('',(22.860912703474,-27.9969516727951,50.));
#9583=CARTESIAN_POINT('',(31.2720779386421,-21.,51.));
#9584=CARTESIAN_POINT('Origin',(30.857864376269,-20.,51.));
#9585=CARTESIAN_POINT('',(23.5680194846605,-28.7040584539816,51.));
#9586=CARTESIAN_POINT('Origin',(49.,-10.5,51.));
#9587=CARTESIAN_POINT('',(50.,45.,51.));
#9588=CARTESIAN_POINT('',(50.,-16.,51.));
#9589=CARTESIAN_POINT('',(50.,-10.5,51.));
#9590=CARTESIAN_POINT('',(49.,-15.5857864376269,50.));
#9591=CARTESIAN_POINT('Origin',(49.,-15.5857864376269,51.));
#9592=CARTESIAN_POINT('',(49.,44.5857864376269,50.));
#9593=CARTESIAN_POINT('',(49.,-10.5,50.));
#9594=CARTESIAN_POINT('Origin',(49.,44.5857864376269,51.));
#9595=CARTESIAN_POINT('Origin',(15.6360389693211,-20.,51.));
#9596=CARTESIAN_POINT('',(44.5857864376269,-20.,50.));
#9597=CARTESIAN_POINT('',(15.6360389693211,-20.,50.));
#9598=CARTESIAN_POINT('',(45.,-21.,51.));
#9599=CARTESIAN_POINT('Origin',(44.5857864376269,-20.,51.));
#9600=CARTESIAN_POINT('',(15.6360389693211,-21.,51.));
#9601=CARTESIAN_POINT('Origin',(39.5428932188134,-25.0428932188135,51.));
#9602=CARTESIAN_POINT('',(40.25,-25.75,51.));
#9603=CARTESIAN_POINT('',(39.5428932188134,-25.0428932188135,50.));
#9604=CARTESIAN_POINT('Origin',(48.0428932188135,45.5428932188135,51.));
#9605=CARTESIAN_POINT('',(45.,50.,51.));
#9606=CARTESIAN_POINT('',(48.75,46.25,51.));
#9607=CARTESIAN_POINT('',(44.5857864376269,49.,50.));
#9608=CARTESIAN_POINT('',(48.0428932188135,45.5428932188135,50.));
#9609=CARTESIAN_POINT('Origin',(44.5857864376269,49.,51.));
#9610=CARTESIAN_POINT('Origin',(22.5,49.,51.));
#9611=CARTESIAN_POINT('',(-45.,50.,51.));
#9612=CARTESIAN_POINT('',(22.5,50.,51.));
#9613=CARTESIAN_POINT('',(-44.5857864376269,49.,50.));
#9614=CARTESIAN_POINT('',(22.5,49.,50.));
#9615=CARTESIAN_POINT('Origin',(-44.5857864376269,49.,51.));
#9616=CARTESIAN_POINT('Origin',(25.0428932188134,-39.5428932188134,51.));
#9617=CARTESIAN_POINT('',(25.0428932188134,-39.5428932188134,50.));
#9618=CARTESIAN_POINT('',(25.75,-40.25,51.));
#9619=CARTESIAN_POINT('Origin',(-45.5428932188135,48.0428932188135,51.));
#9620=CARTESIAN_POINT('',(-50.,45.,51.));
#9621=CARTESIAN_POINT('',(-46.25,48.75,51.));
#9622=CARTESIAN_POINT('',(-49.,44.5857864376269,50.));
#9623=CARTESIAN_POINT('',(-45.5428932188135,48.0428932188135,50.));
#9624=CARTESIAN_POINT('Origin',(-49.,44.5857864376269,51.));
#9625=CARTESIAN_POINT('Origin',(-49.,22.5,51.));
#9626=CARTESIAN_POINT('',(-50.,-45.,51.));
#9627=CARTESIAN_POINT('',(-50.,22.5,51.));
#9628=CARTESIAN_POINT('',(-49.,-44.5857864376269,50.));
#9629=CARTESIAN_POINT('',(-49.,22.5,50.));
#9630=CARTESIAN_POINT('Origin',(-49.,-44.5857864376269,51.));
#9631=CARTESIAN_POINT('Origin',(-48.0428932188135,-45.5428932188135,51.));
#9632=CARTESIAN_POINT('',(-48.75,-46.25,51.));
#9633=CARTESIAN_POINT('',(-48.0428932188135,-45.5428932188135,50.));
#9634=CARTESIAN_POINT('Origin',(18.5,-47.5,50.));
#9635=CARTESIAN_POINT('',(21.,-45.,61.));
#9636=CARTESIAN_POINT('',(21.,-45.,50.));
#9637=CARTESIAN_POINT('',(16.,-50.,61.));
#9638=CARTESIAN_POINT('',(25.75,-40.25,61.));
#9639=CARTESIAN_POINT('',(16.,-50.,50.));
#9640=CARTESIAN_POINT('Origin',(21.,-50.,50.));
#9641=CARTESIAN_POINT('',(21.,-31.2720779386421,61.));
#9642=CARTESIAN_POINT('',(21.,-31.2720779386421,50.));
#9643=CARTESIAN_POINT('',(21.,-25.,61.));
#9644=CARTESIAN_POINT('Origin',(21.,-31.2720779386421,50.));
#9645=CARTESIAN_POINT('',(31.2720779386421,-21.,61.));
#9646=CARTESIAN_POINT('',(31.2720779386421,-21.,50.));
#9647=CARTESIAN_POINT('',(23.5680194846605,-28.7040584539816,61.));
#9648=CARTESIAN_POINT('Origin',(31.2720779386421,-21.,50.));
#9649=CARTESIAN_POINT('',(45.,-21.,61.));
#9650=CARTESIAN_POINT('',(45.,-21.,50.));
#9651=CARTESIAN_POINT('',(15.6360389693211,-21.,61.));
#9652=CARTESIAN_POINT('Origin',(47.5,-18.5,50.));
#9653=CARTESIAN_POINT('',(50.,-16.,61.));
#9654=CARTESIAN_POINT('',(50.,-16.,50.));
#9655=CARTESIAN_POINT('',(40.25,-25.75,61.));
#9656=CARTESIAN_POINT('Origin',(50.,-21.,50.));
#9657=CARTESIAN_POINT('',(50.,45.,61.));
#9658=CARTESIAN_POINT('',(50.,45.,50.));
#9659=CARTESIAN_POINT('',(50.,-10.5,61.));
#9660=CARTESIAN_POINT('Origin',(0.,0.,50.));
#9661=CARTESIAN_POINT('Origin',(-48.0428932188135,-45.5428932188135,61.));
#9662=CARTESIAN_POINT('',(-44.5857864376269,-49.,62.));
#9663=CARTESIAN_POINT('',(-49.,-44.5857864376269,62.));
#9664=CARTESIAN_POINT('',(-48.0428932188135,-45.5428932188135,62.));
#9665=CARTESIAN_POINT('',(-50.,-45.,61.));
#9666=CARTESIAN_POINT('Origin',(-49.,-44.5857864376269,61.));
#9667=CARTESIAN_POINT('',(-45.,-50.,61.));
#9668=CARTESIAN_POINT('',(-48.75,-46.25,61.));
#9669=CARTESIAN_POINT('Origin',(-44.5857864376269,-49.,61.));
#9670=CARTESIAN_POINT('Origin',(-49.,22.5,61.));
#9671=CARTESIAN_POINT('',(-49.,44.5857864376269,62.));
#9672=CARTESIAN_POINT('',(-49.,22.5,62.));
#9673=CARTESIAN_POINT('',(-50.,45.,61.));
#9674=CARTESIAN_POINT('Origin',(-49.,44.5857864376269,61.));
#9675=CARTESIAN_POINT('',(-50.,22.5,61.));
#9676=CARTESIAN_POINT('Origin',(-45.5428932188135,48.0428932188135,61.));
#9677=CARTESIAN_POINT('',(-44.5857864376269,49.,62.));
#9678=CARTESIAN_POINT('',(-45.5428932188135,48.0428932188135,62.));
#9679=CARTESIAN_POINT('',(-45.,50.,61.));
#9680=CARTESIAN_POINT('Origin',(-44.5857864376269,49.,61.));
#9681=CARTESIAN_POINT('',(-46.25,48.75,61.));
#9682=CARTESIAN_POINT('Origin',(22.5,49.,61.));
#9683=CARTESIAN_POINT('',(44.5857864376269,49.,62.));
#9684=CARTESIAN_POINT('',(22.5,49.,62.));
#9685=CARTESIAN_POINT('',(45.,50.,61.));
#9686=CARTESIAN_POINT('Origin',(44.5857864376269,49.,61.));
#9687=CARTESIAN_POINT('',(22.5,50.,61.));
#9688=CARTESIAN_POINT('Origin',(48.0428932188135,45.5428932188135,61.));
#9689=CARTESIAN_POINT('',(49.,44.5857864376269,62.));
#9690=CARTESIAN_POINT('',(48.0428932188135,45.5428932188135,62.));
#9691=CARTESIAN_POINT('Origin',(49.,44.5857864376269,61.));
#9692=CARTESIAN_POINT('',(48.75,46.25,61.));
#9693=CARTESIAN_POINT('Origin',(49.,-10.5,61.));
#9694=CARTESIAN_POINT('',(49.,-15.5857864376269,62.));
#9695=CARTESIAN_POINT('',(49.,-10.5,62.));
#9696=CARTESIAN_POINT('Origin',(49.,-15.5857864376269,61.));
#9697=CARTESIAN_POINT('Origin',(39.5428932188134,-25.0428932188135,61.));
#9698=CARTESIAN_POINT('',(44.5857864376269,-20.,62.));
#9699=CARTESIAN_POINT('',(39.5428932188134,-25.0428932188135,62.));
#9700=CARTESIAN_POINT('Origin',(44.5857864376269,-20.,61.));
#9701=CARTESIAN_POINT('Origin',(15.6360389693211,-20.,61.));
#9702=CARTESIAN_POINT('',(30.857864376269,-20.,62.));
#9703=CARTESIAN_POINT('',(15.6360389693211,-20.,62.));
#9704=CARTESIAN_POINT('Origin',(30.857864376269,-20.,61.));
#9705=CARTESIAN_POINT('Origin',(22.860912703474,-27.9969516727951,61.));
#9706=CARTESIAN_POINT('',(20.,-30.8578643762691,62.));
#9707=CARTESIAN_POINT('',(22.860912703474,-27.9969516727951,62.));
#9708=CARTESIAN_POINT('Origin',(20.,-30.8578643762691,61.));
#9709=CARTESIAN_POINT('Origin',(20.,-25.,61.));
#9710=CARTESIAN_POINT('',(20.,-44.5857864376269,62.));
#9711=CARTESIAN_POINT('',(20.,-25.,62.));
#9712=CARTESIAN_POINT('Origin',(20.,-44.5857864376269,61.));
#9713=CARTESIAN_POINT('Origin',(25.0428932188134,-39.5428932188134,61.));
#9714=CARTESIAN_POINT('',(15.5857864376269,-49.,62.));
#9715=CARTESIAN_POINT('',(25.0428932188134,-39.5428932188134,62.));
#9716=CARTESIAN_POINT('Origin',(15.5857864376269,-49.,61.));
#9717=CARTESIAN_POINT('Origin',(-22.5,-49.,61.));
#9718=CARTESIAN_POINT('',(-22.5,-50.,61.));
#9719=CARTESIAN_POINT('',(-22.5,-49.,62.));
#9720=CARTESIAN_POINT('Origin',(-45.,-50.,50.));
#9721=CARTESIAN_POINT('',(-45.,-50.,50.));
#9722=CARTESIAN_POINT('Origin',(-50.,-45.,50.));
#9723=CARTESIAN_POINT('',(-50.,-45.,50.));
#9724=CARTESIAN_POINT('Origin',(0.,0.,62.));
#9725=CARTESIAN_POINT('Origin',(-50.,45.,50.));
#9726=CARTESIAN_POINT('',(-50.,45.,50.));
#9727=CARTESIAN_POINT('Origin',(-45.,50.,50.));
#9728=CARTESIAN_POINT('',(-45.,50.,50.));
#9729=CARTESIAN_POINT('Origin',(45.,50.,50.));
#9730=CARTESIAN_POINT('',(45.,50.,50.));
#9731=CARTESIAN_POINT('Origin',(50.,45.,50.));
#10116=UNCERTAINTY_MEASURE_WITH_UNIT(LENGTH_MEASURE(0.01),#10132,
'DISTANCE_ACCURACY_VALUE',
'Maximum model space distance between geometric entities at asserted c
onnectivities');
#10119=UNCERTAINTY_MEASURE_WITH_UNIT(LENGTH_MEASURE(0.01),#10132,
'DISTANCE_ACCURACY_VALUE',
'Maximum model space distance between geometric entities at asserted c
onnectivities');
#10128=(
GEOMETRIC_REPRESENTATION_CONTEXT(3)
GLOBAL_UNCERTAINTY_ASSIGNED_CONTEXT((#10116))
GLOBAL_UNIT_ASSIGNED_CONTEXT((#10132,#10134,#10135))
REPRESENTATION_CONTEXT('','3D')
);
#10131=(
GEOMETRIC_REPRESENTATION_CONTEXT(3)
GLOBAL_UNCERTAINTY_ASSIGNED_CONTEXT((#10119))
GLOBAL_UNIT_ASSIGNED_CONTEXT((#10132,#10134,#10135))
REPRESENTATION_CONTEXT('','3D')
);
#10132=(
LENGTH_UNIT()
NAMED_UNIT(*)
SI_UNIT(.MILLI.,.METRE.)
);
#10134=(
NAMED_UNIT(*)
PLANE_ANGLE_UNIT()
SI_UNIT($,.RADIAN.)
);
#10135=(
NAMED_UNIT(*)
SI_UNIT($,.STERADIAN.)
SOLID_ANGLE_UNIT()
);
#10144=SHAPE_DEFINITION_REPRESENTATION(#10155,#10176);
#10155=PRODUCT_DEFINITION_SHAPE('',$,#10188);
#10176=SHAPE_REPRESENTATION('',(#6399),#10128);
#10179=PRODUCT_DEFINITION_CONTEXT('part definition',#10214,'design');
#10188=PRODUCT_DEFINITION('Middle_Block_01','Middle_Block_01',#10199,#10179);
#10199=PRODUCT_DEFINITION_FORMATION('',$,#10224);
#10214=APPLICATION_CONTEXT(
'Core Data for Automotive Mechanical Design Process');
#10215=PRODUCT_CONTEXT('part definition',#10214,'mechanical');
#10224=PRODUCT('Middle_Block_01','Middle_Block_01',$,(#10215));
#10241=COLOUR_RGB('Dark Blue',0.08,0.2,0.34);
#10242=FILL_AREA_STYLE_COLOUR('',#10241);
#10243=FILL_AREA_STYLE('',(#10242));
#10244=SURFACE_STYLE_FILL_AREA(#10243);
#10245=SURFACE_SIDE_STYLE('',(#10244));
#10246=SURFACE_STYLE_USAGE(.BOTH.,#10245);
#10247=PRESENTATION_STYLE_ASSIGNMENT((#10246));
ENDSEC;
END-ISO-10303-21;
